ISO-10303-21;
HEADER;
/* Generated by software containing ST-Developer
 * from STEP Tools, Inc. (www.steptools.com) 
 */

FILE_DESCRIPTION(
/* description */ ('Independent six-slot Geneva indexer. Center distance100, drive radius
50, 60degree indexing per input revolution with120degree engagement an
d240degree dwell. Native machined concave locking faces and relieved d
isk; replaceable retained drive pin; keyed output shaft. Geometry traj
ectory checks use calculated indexing positions, not a contact-dynamic
s simulation. No load or production rating assigned.'),
/* implementation_level */ '2;1');

FILE_NAME(
/* name */ 'Pivot washer.step',
/* time_stamp */ '2026-11-09T17:53:22-08:00',
/* author */ (''),
/* organization */ (''),
/* preprocessor_version */ 'ST-DEVELOPER v20.2',
/* originating_system */ 'Autodesk Translation Framework v15.17.0.0',
/* authorisation */ '');

FILE_SCHEMA (('AUTOMOTIVE_DESIGN { 1 0 10303 214 3 1 1 }'));
ENDSEC;

DATA;
#10=MECHANICAL_DESIGN_GEOMETRIC_PRESENTATION_REPRESENTATION('',(#110),#4149);
#88=SHAPE_REPRESENTATION_RELATIONSHIP('SRR','None',#4205,#99);
#99=ADVANCED_BREP_SHAPE_REPRESENTATION('',(#121),#4147);
#110=STYLED_ITEM('',(#4267),#121);
#121=MANIFOLD_SOLID_BREP('Body1',#2304);
#159=FACE_BOUND('',#539,.T.);
#160=FACE_BOUND('',#541,.T.);
#232=PLANE('',#2687);
#233=PLANE('',#2688);
#364=FACE_OUTER_BOUND('',#536,.T.);
#365=FACE_OUTER_BOUND('',#537,.T.);
#366=FACE_OUTER_BOUND('',#538,.T.);
#367=FACE_OUTER_BOUND('',#540,.T.);
#536=EDGE_LOOP('',(#2064,#2065,#2066,#2067));
#537=EDGE_LOOP('',(#2068,#2069,#2070,#2071));
#538=EDGE_LOOP('',(#2072));
#539=EDGE_LOOP('',(#2073));
#540=EDGE_LOOP('',(#2074));
#541=EDGE_LOOP('',(#2075));
#710=LINE('',#4070,#882);
#711=LINE('',#4076,#883);
#882=VECTOR('',#3389,5.);
#883=VECTOR('',#3396,10.);
#1008=CIRCLE('',#2682,5.);
#1009=CIRCLE('',#2683,5.);
#1010=CIRCLE('',#2685,10.);
#1011=CIRCLE('',#2686,10.);
#1200=VERTEX_POINT('',#4067);
#1201=VERTEX_POINT('',#4069);
#1202=VERTEX_POINT('',#4073);
#1203=VERTEX_POINT('',#4075);
#1490=EDGE_CURVE('',#1200,#1200,#1008,.T.);
#1491=EDGE_CURVE('',#1200,#1201,#710,.T.);
#1492=EDGE_CURVE('',#1201,#1201,#1009,.T.);
#1493=EDGE_CURVE('',#1202,#1202,#1010,.T.);
#1494=EDGE_CURVE('',#1202,#1203,#711,.T.);
#1495=EDGE_CURVE('',#1203,#1203,#1011,.T.);
#2064=ORIENTED_EDGE('',*,*,#1490,.F.);
#2065=ORIENTED_EDGE('',*,*,#1491,.T.);
#2066=ORIENTED_EDGE('',*,*,#1492,.T.);
#2067=ORIENTED_EDGE('',*,*,#1491,.F.);
#2068=ORIENTED_EDGE('',*,*,#1493,.F.);
#2069=ORIENTED_EDGE('',*,*,#1494,.T.);
#2070=ORIENTED_EDGE('',*,*,#1495,.T.);
#2071=ORIENTED_EDGE('',*,*,#1494,.F.);
#2072=ORIENTED_EDGE('',*,*,#1493,.T.);
#2073=ORIENTED_EDGE('',*,*,#1490,.T.);
#2074=ORIENTED_EDGE('',*,*,#1495,.F.);
#2075=ORIENTED_EDGE('',*,*,#1492,.F.);
#2155=CYLINDRICAL_SURFACE('',#2681,5.);
#2156=CYLINDRICAL_SURFACE('',#2684,10.);
#2285=ADVANCED_FACE('',(#364),#2155,.F.);
#2286=ADVANCED_FACE('',(#365),#2156,.T.);
#2287=ADVANCED_FACE('',(#366,#159),#232,.T.);
#2288=ADVANCED_FACE('',(#367,#160),#233,.F.);
#2304=CLOSED_SHELL('',(#2285,#2286,#2287,#2288));
#2680=AXIS2_PLACEMENT_3D('',#4065,#3383,#3384);
#2681=AXIS2_PLACEMENT_3D('',#4066,#3385,#3386);
#2682=AXIS2_PLACEMENT_3D('',#4068,#3387,#3388);
#2683=AXIS2_PLACEMENT_3D('',#4071,#3390,#3391);
#2684=AXIS2_PLACEMENT_3D('',#4072,#3392,#3393);
#2685=AXIS2_PLACEMENT_3D('',#4074,#3394,#3395);
#2686=AXIS2_PLACEMENT_3D('',#4077,#3397,#3398);
#2687=AXIS2_PLACEMENT_3D('',#4078,#3399,#3400);
#2688=AXIS2_PLACEMENT_3D('',#4079,#3401,#3402);
#3383=DIRECTION('axis',(0.,0.,1.));
#3384=DIRECTION('refdir',(1.,0.,0.));
#3385=DIRECTION('center_axis',(0.,0.,1.));
#3386=DIRECTION('ref_axis',(1.,0.,0.));
#3387=DIRECTION('center_axis',(0.,0.,-1.));
#3388=DIRECTION('ref_axis',(1.,0.,0.));
#3389=DIRECTION('',(0.,0.,-1.));
#3390=DIRECTION('center_axis',(0.,0.,-1.));
#3391=DIRECTION('ref_axis',(1.,0.,0.));
#3392=DIRECTION('center_axis',(0.,0.,1.));
#3393=DIRECTION('ref_axis',(1.,0.,0.));
#3394=DIRECTION('center_axis',(0.,0.,1.));
#3395=DIRECTION('ref_axis',(1.,0.,0.));
#3396=DIRECTION('',(0.,0.,-1.));
#3397=DIRECTION('center_axis',(0.,0.,1.));
#3398=DIRECTION('ref_axis',(1.,0.,0.));
#3399=DIRECTION('center_axis',(0.,0.,1.));
#3400=DIRECTION('ref_axis',(1.,0.,0.));
#3401=DIRECTION('center_axis',(0.,0.,1.));
#3402=DIRECTION('ref_axis',(1.,0.,0.));
#4065=CARTESIAN_POINT('',(0.,0.,0.));
#4066=CARTESIAN_POINT('Origin',(0.,0.,0.));
#4067=CARTESIAN_POINT('',(-5.,-6.12323399573677E-16,2.));
#4068=CARTESIAN_POINT('Origin',(0.,0.,2.));
#4069=CARTESIAN_POINT('',(-5.,-6.12323399573677E-16,0.));
#4070=CARTESIAN_POINT('',(-5.,-6.12323399573677E-16,0.));
#4071=CARTESIAN_POINT('Origin',(0.,0.,0.));
#4072=CARTESIAN_POINT('Origin',(0.,0.,0.));
#4073=CARTESIAN_POINT('',(-10.,-1.22464679914735E-15,2.));
#4074=CARTESIAN_POINT('Origin',(0.,0.,2.));
#4075=CARTESIAN_POINT('',(-10.,-1.22464679914735E-15,0.));
#4076=CARTESIAN_POINT('',(-10.,-1.22464679914735E-15,0.));
#4077=CARTESIAN_POINT('Origin',(0.,0.,0.));
#4078=CARTESIAN_POINT('Origin',(0.,0.,2.));
#4079=CARTESIAN_POINT('Origin',(0.,0.,0.));
#4134=UNCERTAINTY_MEASURE_WITH_UNIT(LENGTH_MEASURE(0.01),#4150,
'DISTANCE_ACCURACY_VALUE',
'Maximum model space distance between geometric entities at asserted c
onnectivities');
#4136=UNCERTAINTY_MEASURE_WITH_UNIT(LENGTH_MEASURE(0.01),#4150,
'DISTANCE_ACCURACY_VALUE',
'Maximum model space distance between geometric entities at asserted c
onnectivities');
#4147=(
GEOMETRIC_REPRESENTATION_CONTEXT(3)
GLOBAL_UNCERTAINTY_ASSIGNED_CONTEXT((#4134))
GLOBAL_UNIT_ASSIGNED_CONTEXT((#4150,#4152,#4153))
REPRESENTATION_CONTEXT('','3D')
);
#4149=(
GEOMETRIC_REPRESENTATION_CONTEXT(3)
GLOBAL_UNCERTAINTY_ASSIGNED_CONTEXT((#4136))
GLOBAL_UNIT_ASSIGNED_CONTEXT((#4150,#4152,#4153))
REPRESENTATION_CONTEXT('','3D')
);
#4150=(
LENGTH_UNIT()
NAMED_UNIT(*)
SI_UNIT(.MILLI.,.METRE.)
);
#4152=(
NAMED_UNIT(*)
PLANE_ANGLE_UNIT()
SI_UNIT($,.RADIAN.)
);
#4153=(
NAMED_UNIT(*)
SI_UNIT($,.STERADIAN.)
SOLID_ANGLE_UNIT()
);
#4164=SHAPE_DEFINITION_REPRESENTATION(#4176,#4205);
#4176=PRODUCT_DEFINITION_SHAPE('',$,#4218);
#4205=SHAPE_REPRESENTATION('',(#2680),#4147);
#4207=PRODUCT_DEFINITION_CONTEXT('part definition',#4245,'design');
#4218=PRODUCT_DEFINITION('Pivot washer','Pivot washer',#4230,#4207);
#4230=PRODUCT_DEFINITION_FORMATION('',$,#4257);
#4245=APPLICATION_CONTEXT(
'Core Data for Automotive Mechanical Design Process');
#4246=PRODUCT_CONTEXT('part definition',#4245,'mechanical');
#4257=PRODUCT('Pivot washer','Pivot washer',$,(#4246));
#4267=PRESENTATION_STYLE_ASSIGNMENT((#4277));
#4277=SURFACE_STYLE_USAGE(.BOTH.,#4287);
#4287=SURFACE_SIDE_STYLE('',(#4297));
#4297=SURFACE_STYLE_FILL_AREA(#4307);
#4307=FILL_AREA_STYLE('Washer light gray',(#4317));
#4317=FILL_AREA_STYLE_COLOUR('Washer light gray',#4327);
#4327=COLOUR_RGB('Washer light gray',0.725490196078431,0.752941176470588,
0.792156862745098);
ENDSEC;
END-ISO-10303-21;
